ISO-10303-21;
HEADER;
/* Generated by software containing ST-Developer
 * from STEP Tools, Inc. (www.steptools.com) 
 */

FILE_DESCRIPTION(
/* description */ (''),
/* implementation_level */ '2;1');

FILE_NAME(
/* name */ 'Hex Nut - M8.step',
/* time_stamp */ '2026-10-29T16:43:51-07:00',
/* author */ (''),
/* organization */ (''),
/* preprocessor_version */ 'ST-DEVELOPER v20.2',
/* originating_system */ 'Autodesk Translation Framework v15.17.0.0',
/* authorisation */ '');

FILE_SCHEMA (('AUTOMOTIVE_DESIGN { 1 0 10303 214 3 1 1 }'));
ENDSEC;

DATA;
#10=MECHANICAL_DESIGN_GEOMETRIC_PRESENTATION_REPRESENTATION('',(#374),#10292);
#271=(
BOUNDED_CURVE()
B_SPLINE_CURVE(2,(#8041,#8042,#8043),.UNSPECIFIED.,.F.,.F.)
B_SPLINE_CURVE_WITH_KNOTS((3,3),(0.14973948338295,0.97160236658079),
 .UNSPECIFIED.)
CURVE()
GEOMETRIC_REPRESENTATION_ITEM()
RATIONAL_B_SPLINE_CURVE((1.07140024848292,1.23714644374248,1.07140024848292))
REPRESENTATION_ITEM('')
);
#272=(
BOUNDED_CURVE()
B_SPLINE_CURVE(2,(#8045,#8046,#8047),.UNSPECIFIED.,.F.,.F.)
B_SPLINE_CURVE_WITH_KNOTS((3,3),(0.14973948338295,0.971602366580789),
 .UNSPECIFIED.)
CURVE()
GEOMETRIC_REPRESENTATION_ITEM()
RATIONAL_B_SPLINE_CURVE((1.07140024848292,1.23714644374248,1.07140024848292))
REPRESENTATION_ITEM('')
);
#273=(
BOUNDED_CURVE()
B_SPLINE_CURVE(2,(#8052,#8053,#8054),.UNSPECIFIED.,.F.,.F.)
B_SPLINE_CURVE_WITH_KNOTS((3,3),(0.14973948338295,0.97160236658079),
 .UNSPECIFIED.)
CURVE()
GEOMETRIC_REPRESENTATION_ITEM()
RATIONAL_B_SPLINE_CURVE((1.07140024848292,1.23714644374248,1.07140024848292))
REPRESENTATION_ITEM('')
);
#274=(
BOUNDED_CURVE()
B_SPLINE_CURVE(2,(#8056,#8057,#8058),.UNSPECIFIED.,.F.,.F.)
B_SPLINE_CURVE_WITH_KNOTS((3,3),(0.14973948338295,0.97160236658079),
 .UNSPECIFIED.)
CURVE()
GEOMETRIC_REPRESENTATION_ITEM()
RATIONAL_B_SPLINE_CURVE((1.07140024848292,1.23714644374248,1.07140024848292))
REPRESENTATION_ITEM('')
);
#275=(
BOUNDED_CURVE()
B_SPLINE_CURVE(2,(#8060,#8061,#8062),.UNSPECIFIED.,.F.,.F.)
B_SPLINE_CURVE_WITH_KNOTS((3,3),(0.14973948338295,0.971602366580789),
 .UNSPECIFIED.)
CURVE()
GEOMETRIC_REPRESENTATION_ITEM()
RATIONAL_B_SPLINE_CURVE((1.07140024848292,1.23714644374248,1.07140024848292))
REPRESENTATION_ITEM('')
);
#276=(
BOUNDED_CURVE()
B_SPLINE_CURVE(2,(#8063,#8064,#8065),.UNSPECIFIED.,.F.,.F.)
B_SPLINE_CURVE_WITH_KNOTS((3,3),(0.14973948338295,0.97160236658079),
 .UNSPECIFIED.)
CURVE()
GEOMETRIC_REPRESENTATION_ITEM()
RATIONAL_B_SPLINE_CURVE((1.07140024848292,1.23714644374248,1.07140024848292))
REPRESENTATION_ITEM('')
);
#277=(
BOUNDED_CURVE()
B_SPLINE_CURVE(2,(#8072,#8073,#8074),.UNSPECIFIED.,.F.,.F.)
B_SPLINE_CURVE_WITH_KNOTS((3,3),(0.14973948338295,0.97160236658079),
 .UNSPECIFIED.)
CURVE()
GEOMETRIC_REPRESENTATION_ITEM()
RATIONAL_B_SPLINE_CURVE((1.07140024848292,1.23714644374248,1.07140024848292))
REPRESENTATION_ITEM('')
);
#278=(
BOUNDED_CURVE()
B_SPLINE_CURVE(2,(#8076,#8077,#8078),.UNSPECIFIED.,.F.,.F.)
B_SPLINE_CURVE_WITH_KNOTS((3,3),(0.14973948338295,0.97160236658079),
 .UNSPECIFIED.)
CURVE()
GEOMETRIC_REPRESENTATION_ITEM()
RATIONAL_B_SPLINE_CURVE((1.07140024848292,1.23714644374248,1.07140024848292))
REPRESENTATION_ITEM('')
);
#279=(
BOUNDED_CURVE()
B_SPLINE_CURVE(2,(#8080,#8081,#8082),.UNSPECIFIED.,.F.,.F.)
B_SPLINE_CURVE_WITH_KNOTS((3,3),(0.14973948338295,0.971602366580789),
 .UNSPECIFIED.)
CURVE()
GEOMETRIC_REPRESENTATION_ITEM()
RATIONAL_B_SPLINE_CURVE((1.07140024848292,1.23714644374248,1.07140024848292))
REPRESENTATION_ITEM('')
);
#280=(
BOUNDED_CURVE()
B_SPLINE_CURVE(2,(#8084,#8085,#8086),.UNSPECIFIED.,.F.,.F.)
B_SPLINE_CURVE_WITH_KNOTS((3,3),(0.14973948338295,0.97160236658079),
 .UNSPECIFIED.)
CURVE()
GEOMETRIC_REPRESENTATION_ITEM()
RATIONAL_B_SPLINE_CURVE((1.07140024848292,1.23714644374248,1.07140024848292))
REPRESENTATION_ITEM('')
);
#281=(
BOUNDED_CURVE()
B_SPLINE_CURVE(2,(#8088,#8089,#8090),.UNSPECIFIED.,.F.,.F.)
B_SPLINE_CURVE_WITH_KNOTS((3,3),(0.14973948338295,0.97160236658079),
 .UNSPECIFIED.)
CURVE()
GEOMETRIC_REPRESENTATION_ITEM()
RATIONAL_B_SPLINE_CURVE((1.07140024848292,1.23714644374248,1.07140024848292))
REPRESENTATION_ITEM('')
);
#282=(
BOUNDED_CURVE()
B_SPLINE_CURVE(2,(#8091,#8092,#8093),.UNSPECIFIED.,.F.,.F.)
B_SPLINE_CURVE_WITH_KNOTS((3,3),(0.14973948338295,0.971602366580789),
 .UNSPECIFIED.)
CURVE()
GEOMETRIC_REPRESENTATION_ITEM()
RATIONAL_B_SPLINE_CURVE((1.07140024848292,1.23714644374248,1.07140024848292))
REPRESENTATION_ITEM('')
);
#303=CONICAL_SURFACE('',#5515,0.734027674973257,1.0471975511966);
#304=CONICAL_SURFACE('',#5517,0.734027674973257,1.0471975511966);
#328=SHAPE_REPRESENTATION_RELATIONSHIP('SRR','None',#10424,#351);
#351=ADVANCED_BREP_SHAPE_REPRESENTATION('',(#395),#10276);
#374=STYLED_ITEM('',(#10635),#395);
#395=MANIFOLD_SOLID_BREP('Body1',#5018);
#468=FACE_BOUND('',#1198,.T.);
#469=FACE_BOUND('',#1200,.T.);
#611=PLANE('',#5519);
#612=PLANE('',#5520);
#613=PLANE('',#5521);
#614=PLANE('',#5525);
#615=PLANE('',#5526);
#616=PLANE('',#5527);
#617=PLANE('',#5528);
#618=PLANE('',#5529);
#838=FACE_OUTER_BOUND('',#1188,.T.);
#839=FACE_OUTER_BOUND('',#1189,.T.);
#840=FACE_OUTER_BOUND('',#1190,.T.);
#841=FACE_OUTER_BOUND('',#1191,.T.);
#842=FACE_OUTER_BOUND('',#1192,.T.);
#843=FACE_OUTER_BOUND('',#1193,.T.);
#844=FACE_OUTER_BOUND('',#1194,.T.);
#845=FACE_OUTER_BOUND('',#1195,.T.);
#846=FACE_OUTER_BOUND('',#1196,.T.);
#847=FACE_OUTER_BOUND('',#1197,.T.);
#848=FACE_OUTER_BOUND('',#1199,.T.);
#1188=EDGE_LOOP('',(#3989,#3990,#3991,#3992,#3993,#3994,#3995,#3996,#3997));
#1189=EDGE_LOOP('',(#3998,#3999,#4000,#4001,#4002,#4003,#4004,#4005,#4006));
#1190=EDGE_LOOP('',(#4007,#4008,#4009,#4010));
#1191=EDGE_LOOP('',(#4011,#4012,#4013,#4014));
#1192=EDGE_LOOP('',(#4015,#4016,#4017,#4018));
#1193=EDGE_LOOP('',(#4019,#4020,#4021,#4022));
#1194=EDGE_LOOP('',(#4023,#4024,#4025,#4026));
#1195=EDGE_LOOP('',(#4027,#4028,#4029,#4030));
#1196=EDGE_LOOP('',(#4031,#4032,#4033,#4034));
#1197=EDGE_LOOP('',(#4035));
#1198=EDGE_LOOP('',(#4036));
#1199=EDGE_LOOP('',(#4037));
#1200=EDGE_LOOP('',(#4038));
#1609=LINE('',#8049,#2001);
#1610=LINE('',#8070,#2002);
#1611=LINE('',#8095,#2003);
#1612=LINE('',#8096,#2004);
#1613=LINE('',#8098,#2005);
#1614=LINE('',#8100,#2006);
#1615=LINE('',#8105,#2007);
#1616=LINE('',#8108,#2008);
#1617=LINE('',#8110,#2009);
#2001=VECTOR('',#6516,0.734027674973257);
#2002=VECTOR('',#6523,0.734027674973257);
#2003=VECTOR('',#6526,1.);
#2004=VECTOR('',#6527,1.);
#2005=VECTOR('',#6530,1.);
#2006=VECTOR('',#6533,1.);
#2007=VECTOR('',#6538,0.4);
#2008=VECTOR('',#6543,1.);
#2009=VECTOR('',#6546,1.);
#2281=CIRCLE('',#5516,0.6175);
#2282=CIRCLE('',#5518,0.6175);
#2283=CIRCLE('',#5523,0.338975);
#2284=CIRCLE('',#5524,0.338975);
#2584=VERTEX_POINT('',#8039);
#2585=VERTEX_POINT('',#8040);
#2586=VERTEX_POINT('',#8044);
#2587=VERTEX_POINT('',#8048);
#2588=VERTEX_POINT('',#8051);
#2589=VERTEX_POINT('',#8055);
#2590=VERTEX_POINT('',#8059);
#2591=VERTEX_POINT('',#8067);
#2592=VERTEX_POINT('',#8069);
#2593=VERTEX_POINT('',#8071);
#2594=VERTEX_POINT('',#8075);
#2595=VERTEX_POINT('',#8079);
#2596=VERTEX_POINT('',#8083);
#2597=VERTEX_POINT('',#8087);
#2598=VERTEX_POINT('',#8102);
#2599=VERTEX_POINT('',#8104);
#3085=EDGE_CURVE('',#2584,#2585,#271,.T.);
#3086=EDGE_CURVE('',#2586,#2584,#272,.T.);
#3087=EDGE_CURVE('',#2586,#2587,#1609,.T.);
#3088=EDGE_CURVE('',#2587,#2587,#2281,.T.);
#3089=EDGE_CURVE('',#2588,#2586,#273,.T.);
#3090=EDGE_CURVE('',#2589,#2588,#274,.T.);
#3091=EDGE_CURVE('',#2590,#2589,#275,.T.);
#3092=EDGE_CURVE('',#2585,#2590,#276,.T.);
#3093=EDGE_CURVE('',#2591,#2591,#2282,.T.);
#3094=EDGE_CURVE('',#2591,#2592,#1610,.T.);
#3095=EDGE_CURVE('',#2593,#2592,#277,.T.);
#3096=EDGE_CURVE('',#2594,#2593,#278,.T.);
#3097=EDGE_CURVE('',#2595,#2594,#279,.T.);
#3098=EDGE_CURVE('',#2596,#2595,#280,.T.);
#3099=EDGE_CURVE('',#2597,#2596,#281,.T.);
#3100=EDGE_CURVE('',#2592,#2597,#282,.T.);
#3101=EDGE_CURVE('',#2588,#2597,#1611,.T.);
#3102=EDGE_CURVE('',#2589,#2596,#1612,.T.);
#3103=EDGE_CURVE('',#2586,#2592,#1613,.T.);
#3104=EDGE_CURVE('',#2584,#2593,#1614,.T.);
#3105=EDGE_CURVE('',#2598,#2598,#2283,.F.);
#3106=EDGE_CURVE('',#2598,#2599,#1615,.T.);
#3107=EDGE_CURVE('',#2599,#2599,#2284,.F.);
#3108=EDGE_CURVE('',#2585,#2594,#1616,.T.);
#3109=EDGE_CURVE('',#2590,#2595,#1617,.T.);
#3989=ORIENTED_EDGE('',*,*,#3085,.F.);
#3990=ORIENTED_EDGE('',*,*,#3086,.F.);
#3991=ORIENTED_EDGE('',*,*,#3087,.T.);
#3992=ORIENTED_EDGE('',*,*,#3088,.F.);
#3993=ORIENTED_EDGE('',*,*,#3087,.F.);
#3994=ORIENTED_EDGE('',*,*,#3089,.F.);
#3995=ORIENTED_EDGE('',*,*,#3090,.F.);
#3996=ORIENTED_EDGE('',*,*,#3091,.F.);
#3997=ORIENTED_EDGE('',*,*,#3092,.F.);
#3998=ORIENTED_EDGE('',*,*,#3093,.F.);
#3999=ORIENTED_EDGE('',*,*,#3094,.T.);
#4000=ORIENTED_EDGE('',*,*,#3095,.F.);
#4001=ORIENTED_EDGE('',*,*,#3096,.F.);
#4002=ORIENTED_EDGE('',*,*,#3097,.F.);
#4003=ORIENTED_EDGE('',*,*,#3098,.F.);
#4004=ORIENTED_EDGE('',*,*,#3099,.F.);
#4005=ORIENTED_EDGE('',*,*,#3100,.F.);
#4006=ORIENTED_EDGE('',*,*,#3094,.F.);
#4007=ORIENTED_EDGE('',*,*,#3090,.T.);
#4008=ORIENTED_EDGE('',*,*,#3101,.T.);
#4009=ORIENTED_EDGE('',*,*,#3099,.T.);
#4010=ORIENTED_EDGE('',*,*,#3102,.F.);
#4011=ORIENTED_EDGE('',*,*,#3089,.T.);
#4012=ORIENTED_EDGE('',*,*,#3103,.T.);
#4013=ORIENTED_EDGE('',*,*,#3100,.T.);
#4014=ORIENTED_EDGE('',*,*,#3101,.F.);
#4015=ORIENTED_EDGE('',*,*,#3086,.T.);
#4016=ORIENTED_EDGE('',*,*,#3104,.T.);
#4017=ORIENTED_EDGE('',*,*,#3095,.T.);
#4018=ORIENTED_EDGE('',*,*,#3103,.F.);
#4019=ORIENTED_EDGE('',*,*,#3105,.F.);
#4020=ORIENTED_EDGE('',*,*,#3106,.T.);
#4021=ORIENTED_EDGE('',*,*,#3107,.T.);
#4022=ORIENTED_EDGE('',*,*,#3106,.F.);
#4023=ORIENTED_EDGE('',*,*,#3085,.T.);
#4024=ORIENTED_EDGE('',*,*,#3108,.T.);
#4025=ORIENTED_EDGE('',*,*,#3096,.T.);
#4026=ORIENTED_EDGE('',*,*,#3104,.F.);
#4027=ORIENTED_EDGE('',*,*,#3091,.T.);
#4028=ORIENTED_EDGE('',*,*,#3102,.T.);
#4029=ORIENTED_EDGE('',*,*,#3098,.T.);
#4030=ORIENTED_EDGE('',*,*,#3109,.F.);
#4031=ORIENTED_EDGE('',*,*,#3092,.T.);
#4032=ORIENTED_EDGE('',*,*,#3109,.T.);
#4033=ORIENTED_EDGE('',*,*,#3097,.T.);
#4034=ORIENTED_EDGE('',*,*,#3108,.F.);
#4035=ORIENTED_EDGE('',*,*,#3093,.T.);
#4036=ORIENTED_EDGE('',*,*,#3105,.T.);
#4037=ORIENTED_EDGE('',*,*,#3088,.T.);
#4038=ORIENTED_EDGE('',*,*,#3107,.F.);
#4675=CYLINDRICAL_SURFACE('',#5522,0.338975);
#4847=ADVANCED_FACE('',(#838),#303,.T.);
#4848=ADVANCED_FACE('',(#839),#304,.T.);
#4849=ADVANCED_FACE('',(#840),#611,.T.);
#4850=ADVANCED_FACE('',(#841),#612,.T.);
#4851=ADVANCED_FACE('',(#842),#613,.T.);
#4852=ADVANCED_FACE('',(#843),#4675,.F.);
#4853=ADVANCED_FACE('',(#844),#614,.T.);
#4854=ADVANCED_FACE('',(#845),#615,.T.);
#4855=ADVANCED_FACE('',(#846),#616,.T.);
#4856=ADVANCED_FACE('',(#847,#468),#617,.T.);
#4857=ADVANCED_FACE('',(#848,#469),#618,.F.);
#5018=CLOSED_SHELL('',(#4847,#4848,#4849,#4850,#4851,#4852,#4853,#4854,
#4855,#4856,#4857));
#5514=AXIS2_PLACEMENT_3D('',#8037,#6512,#6513);
#5515=AXIS2_PLACEMENT_3D('',#8038,#6514,#6515);
#5516=AXIS2_PLACEMENT_3D('',#8050,#6517,#6518);
#5517=AXIS2_PLACEMENT_3D('',#8066,#6519,#6520);
#5518=AXIS2_PLACEMENT_3D('',#8068,#6521,#6522);
#5519=AXIS2_PLACEMENT_3D('',#8094,#6524,#6525);
#5520=AXIS2_PLACEMENT_3D('',#8097,#6528,#6529);
#5521=AXIS2_PLACEMENT_3D('',#8099,#6531,#6532);
#5522=AXIS2_PLACEMENT_3D('',#8101,#6534,#6535);
#5523=AXIS2_PLACEMENT_3D('',#8103,#6536,#6537);
#5524=AXIS2_PLACEMENT_3D('',#8106,#6539,#6540);
#5525=AXIS2_PLACEMENT_3D('',#8107,#6541,#6542);
#5526=AXIS2_PLACEMENT_3D('',#8109,#6544,#6545);
#5527=AXIS2_PLACEMENT_3D('',#8111,#6547,#6548);
#5528=AXIS2_PLACEMENT_3D('',#8112,#6549,#6550);
#5529=AXIS2_PLACEMENT_3D('',#8113,#6551,#6552);
#6512=DIRECTION('axis',(0.,0.,1.));
#6513=DIRECTION('refdir',(1.,0.,0.));
#6514=DIRECTION('center_axis',(0.,1.,0.));
#6515=DIRECTION('ref_axis',(1.,0.,0.));
#6516=DIRECTION('',(0.866025403784439,-0.5,1.06057523872491E-16));
#6517=DIRECTION('center_axis',(0.,-1.,0.));
#6518=DIRECTION('ref_axis',(1.,0.,0.));
#6519=DIRECTION('center_axis',(0.,-1.,0.));
#6520=DIRECTION('ref_axis',(1.,0.,0.));
#6521=DIRECTION('center_axis',(0.,1.,0.));
#6522=DIRECTION('ref_axis',(1.,0.,0.));
#6523=DIRECTION('',(-0.866025403784439,-0.5,-1.06057523872491E-16));
#6524=DIRECTION('center_axis',(1.4792020664489E-16,0.,-1.));
#6525=DIRECTION('ref_axis',(-1.,0.,-1.4792020664489E-16));
#6526=DIRECTION('',(0.,1.,0.));
#6527=DIRECTION('',(0.,1.,0.));
#6528=DIRECTION('center_axis',(-0.866025403784439,0.,-0.5));
#6529=DIRECTION('ref_axis',(-0.5,0.,0.866025403784439));
#6530=DIRECTION('',(0.,1.,0.));
#6531=DIRECTION('center_axis',(-0.866025403784439,0.,0.5));
#6532=DIRECTION('ref_axis',(0.5,0.,0.866025403784439));
#6533=DIRECTION('',(0.,1.,0.));
#6534=DIRECTION('center_axis',(0.,1.,0.));
#6535=DIRECTION('ref_axis',(1.,0.,0.));
#6536=DIRECTION('center_axis',(0.,1.,0.));
#6537=DIRECTION('ref_axis',(1.,0.,0.));
#6538=DIRECTION('',(0.,-1.,0.));
#6539=DIRECTION('center_axis',(0.,1.,0.));
#6540=DIRECTION('ref_axis',(1.,0.,0.));
#6541=DIRECTION('center_axis',(-2.95840413289779E-16,0.,1.));
#6542=DIRECTION('ref_axis',(1.,0.,2.95840413289779E-16));
#6543=DIRECTION('',(0.,1.,0.));
#6544=DIRECTION('center_axis',(0.866025403784439,0.,-0.5));
#6545=DIRECTION('ref_axis',(-0.5,0.,-0.866025403784439));
#6546=DIRECTION('',(0.,1.,0.));
#6547=DIRECTION('center_axis',(0.866025403784439,0.,0.5));
#6548=DIRECTION('ref_axis',(0.5,0.,-0.866025403784439));
#6549=DIRECTION('center_axis',(0.,1.,0.));
#6550=DIRECTION('ref_axis',(1.,0.,0.));
#6551=DIRECTION('center_axis',(0.,1.,0.));
#6552=DIRECTION('ref_axis',(1.,0.,0.));
#8037=CARTESIAN_POINT('',(0.,0.,0.));
#8038=CARTESIAN_POINT('Origin',(0.,0.067277284513851,0.));
#8039=CARTESIAN_POINT('',(-0.375277674973257,0.0768195421087395,0.65));
#8040=CARTESIAN_POINT('',(0.375277674973257,0.0768195421087395,0.65));
#8041=CARTESIAN_POINT('Ctrl Pts',(-0.375277674973257,0.0768195421087395,
0.65));
#8042=CARTESIAN_POINT('Ctrl Pts',(1.66533453693773E-13,-0.0315137912242439,
0.65));
#8043=CARTESIAN_POINT('Ctrl Pts',(0.375277674973257,0.0768195421087394,
0.65));
#8044=CARTESIAN_POINT('',(-0.750555349946514,0.0768195421087394,-9.19165206894919E-17));
#8045=CARTESIAN_POINT('Ctrl Pts',(-0.750555349946514,0.0768195421087394,
-9.19165206894919E-17));
#8046=CARTESIAN_POINT('Ctrl Pts',(-0.562916512459802,-0.0315137912242434,
0.325000000000144));
#8047=CARTESIAN_POINT('Ctrl Pts',(-0.375277674973257,0.0768195421087395,
0.65));
#8048=CARTESIAN_POINT('',(-0.6175,-2.77555756156289E-17,-7.5621939847349E-17));
#8049=CARTESIAN_POINT('',(-0.734027674973257,0.067277284513851,-8.98924642641573E-17));
#8050=CARTESIAN_POINT('Origin',(0.,0.,0.));
#8051=CARTESIAN_POINT('',(-0.375277674973257,0.0768195421087395,-0.65));
#8052=CARTESIAN_POINT('Ctrl Pts',(-0.375277674973257,0.0768195421087395,
-0.65));
#8053=CARTESIAN_POINT('Ctrl Pts',(-0.562916512459968,-0.0315137912242437,
-0.324999999999856));
#8054=CARTESIAN_POINT('Ctrl Pts',(-0.750555349946514,0.0768195421087395,
-9.19165206894919E-17));
#8055=CARTESIAN_POINT('',(0.375277674973257,0.0768195421087395,-0.65));
#8056=CARTESIAN_POINT('Ctrl Pts',(0.375277674973257,0.0768195421087395,
-0.65));
#8057=CARTESIAN_POINT('Ctrl Pts',(-1.66144875635155E-13,-0.0315137912242437,
-0.65));
#8058=CARTESIAN_POINT('Ctrl Pts',(-0.375277674973257,0.0768195421087395,
-0.65));
#8059=CARTESIAN_POINT('',(0.750555349946514,0.0768195421087394,0.));
#8060=CARTESIAN_POINT('Ctrl Pts',(0.750555349946514,0.0768195421087394,
0.));
#8061=CARTESIAN_POINT('Ctrl Pts',(0.562916512459802,-0.0315137912242436,
-0.325000000000144));
#8062=CARTESIAN_POINT('Ctrl Pts',(0.375277674973257,0.0768195421087395,
-0.65));
#8063=CARTESIAN_POINT('Ctrl Pts',(0.375277674973257,0.0768195421087394,
0.65));
#8064=CARTESIAN_POINT('Ctrl Pts',(0.562916512459968,-0.0315137912242439,
0.324999999999856));
#8065=CARTESIAN_POINT('Ctrl Pts',(0.750555349946514,0.0768195421087394,
0.));
#8066=CARTESIAN_POINT('Origin',(0.,0.612722715486149,0.));
#8067=CARTESIAN_POINT('',(-0.6175,0.68,-7.5621939847349E-17));
#8068=CARTESIAN_POINT('Origin',(0.,0.68,0.));
#8069=CARTESIAN_POINT('',(-0.750555349946514,0.603180457891261,-9.19165206894919E-17));
#8070=CARTESIAN_POINT('',(-0.734027674973257,0.612722715486149,-8.98924642641573E-17));
#8071=CARTESIAN_POINT('',(-0.375277674973257,0.603180457891261,0.65));
#8072=CARTESIAN_POINT('Ctrl Pts',(-0.375277674973257,0.603180457891261,
0.65));
#8073=CARTESIAN_POINT('Ctrl Pts',(-0.562916512459968,0.711513791224243,
0.324999999999856));
#8074=CARTESIAN_POINT('Ctrl Pts',(-0.750555349946514,0.603180457891261,
-9.19165206894919E-17));
#8075=CARTESIAN_POINT('',(0.375277674973257,0.603180457891261,0.65));
#8076=CARTESIAN_POINT('Ctrl Pts',(0.375277674973257,0.603180457891261,0.65));
#8077=CARTESIAN_POINT('Ctrl Pts',(-1.66755498298699E-13,0.711513791224244,
0.65));
#8078=CARTESIAN_POINT('Ctrl Pts',(-0.375277674973257,0.603180457891261,
0.65));
#8079=CARTESIAN_POINT('',(0.750555349946514,0.603180457891261,0.));
#8080=CARTESIAN_POINT('Ctrl Pts',(0.750555349946514,0.603180457891261,0.));
#8081=CARTESIAN_POINT('Ctrl Pts',(0.562916512459802,0.711513791224244,0.325000000000144));
#8082=CARTESIAN_POINT('Ctrl Pts',(0.375277674973257,0.603180457891261,0.65));
#8083=CARTESIAN_POINT('',(0.375277674973257,0.603180457891261,-0.65));
#8084=CARTESIAN_POINT('Ctrl Pts',(0.375277674973257,0.603180457891261,-0.65));
#8085=CARTESIAN_POINT('Ctrl Pts',(0.562916512459969,0.711513791224244,-0.324999999999856));
#8086=CARTESIAN_POINT('Ctrl Pts',(0.750555349946514,0.603180457891261,0.));
#8087=CARTESIAN_POINT('',(-0.375277674973257,0.603180457891261,-0.65));
#8088=CARTESIAN_POINT('Ctrl Pts',(-0.375277674973257,0.603180457891261,
-0.65));
#8089=CARTESIAN_POINT('Ctrl Pts',(1.66422431391311E-13,0.711513791224244,
-0.65));
#8090=CARTESIAN_POINT('Ctrl Pts',(0.375277674973257,0.603180457891261,-0.65));
#8091=CARTESIAN_POINT('Ctrl Pts',(-0.750555349946514,0.603180457891261,
-9.19165206894919E-17));
#8092=CARTESIAN_POINT('Ctrl Pts',(-0.562916512459802,0.711513791224244,
-0.325000000000144));
#8093=CARTESIAN_POINT('Ctrl Pts',(-0.375277674973257,0.603180457891261,
-0.65));
#8094=CARTESIAN_POINT('Origin',(0.375277674973257,0.,-0.65));
#8095=CARTESIAN_POINT('',(-0.375277674973257,0.,-0.65));
#8096=CARTESIAN_POINT('',(0.375277674973257,0.,-0.65));
#8097=CARTESIAN_POINT('Origin',(-0.375277674973257,0.,-0.65));
#8098=CARTESIAN_POINT('',(-0.750555349946514,0.,-9.19165206894919E-17));
#8099=CARTESIAN_POINT('Origin',(-0.750555349946514,0.,-9.19165206894919E-17));
#8100=CARTESIAN_POINT('',(-0.375277674973257,0.,0.65));
#8101=CARTESIAN_POINT('Origin',(0.,0.,0.));
#8102=CARTESIAN_POINT('',(-0.338975,0.68,4.15124648740974E-17));
#8103=CARTESIAN_POINT('Origin',(0.,0.68,0.));
#8104=CARTESIAN_POINT('',(-0.338975,0.,4.15124648740974E-17));
#8105=CARTESIAN_POINT('',(-0.338975,0.,4.15124648740974E-17));
#8106=CARTESIAN_POINT('Origin',(0.,0.,0.));
#8107=CARTESIAN_POINT('Origin',(-0.375277674973257,0.,0.65));
#8108=CARTESIAN_POINT('',(0.375277674973257,0.,0.65));
#8109=CARTESIAN_POINT('Origin',(0.750555349946514,0.,0.));
#8110=CARTESIAN_POINT('',(0.750555349946514,0.,0.));
#8111=CARTESIAN_POINT('Origin',(0.375277674973257,0.,0.65));
#8112=CARTESIAN_POINT('Origin',(0.,0.68,-1.11022302462516E-16));
#8113=CARTESIAN_POINT('Origin',(0.,0.,-1.11022302462516E-16));
#10248=UNCERTAINTY_MEASURE_WITH_UNIT(LENGTH_MEASURE(0.001),#10293,
'DISTANCE_ACCURACY_VALUE',
'Maximum model space distance between geometric entities at asserted c
onnectivities');
#10264=UNCERTAINTY_MEASURE_WITH_UNIT(LENGTH_MEASURE(0.001),#10293,
'DISTANCE_ACCURACY_VALUE',
'Maximum model space distance between geometric entities at asserted c
onnectivities');
#10276=(
GEOMETRIC_REPRESENTATION_CONTEXT(3)
GLOBAL_UNCERTAINTY_ASSIGNED_CONTEXT((#10248))
GLOBAL_UNIT_ASSIGNED_CONTEXT((#10293,#10295,#10296))
REPRESENTATION_CONTEXT('','3D')
);
#10292=(
GEOMETRIC_REPRESENTATION_CONTEXT(3)
GLOBAL_UNCERTAINTY_ASSIGNED_CONTEXT((#10264))
GLOBAL_UNIT_ASSIGNED_CONTEXT((#10293,#10295,#10296))
REPRESENTATION_CONTEXT('','3D')
);
#10293=(
LENGTH_UNIT()
NAMED_UNIT(*)
SI_UNIT(.CENTI.,.METRE.)
);
#10295=(
NAMED_UNIT(*)
PLANE_ANGLE_UNIT()
SI_UNIT($,.RADIAN.)
);
#10296=(
NAMED_UNIT(*)
SI_UNIT($,.STERADIAN.)
SOLID_ANGLE_UNIT()
);
#10308=SHAPE_DEFINITION_REPRESENTATION(#10335,#10424);
#10335=PRODUCT_DEFINITION_SHAPE('',$,#10452);
#10424=SHAPE_REPRESENTATION('',(#5514),#10276);
#10440=PRODUCT_DEFINITION_CONTEXT('part definition',#10523,'design');
#10452=PRODUCT_DEFINITION('Hex Nut - M8','Hex Nut - M8',#10479,
#10440);
#10479=PRODUCT_DEFINITION_FORMATION('',$,#10536);
#10523=APPLICATION_CONTEXT(
'Core Data for Automotive Mechanical Design Process');
#10524=PRODUCT_CONTEXT('part definition',#10523,'mechanical');
#10536=PRODUCT('Hex Nut - M8','Hex Nut - M8','Hex Nut - M8',
(#10524));
#10629=COLOUR_RGB('Black',0.12,0.14,0.17);
#10630=FILL_AREA_STYLE_COLOUR('',#10629);
#10631=FILL_AREA_STYLE('',(#10630));
#10632=SURFACE_STYLE_FILL_AREA(#10631);
#10633=SURFACE_SIDE_STYLE('',(#10632));
#10634=SURFACE_STYLE_USAGE(.BOTH.,#10633);
#10635=PRESENTATION_STYLE_ASSIGNMENT((#10634));
ENDSEC;
END-ISO-10303-21;
